ISO-10303-21;
HEADER;
/* Generated by software containing ST-Developer
 * from STEP Tools, Inc. (www.steptools.com) 
 */

FILE_DESCRIPTION(
/* description */ ('PAT-083'),
/* implementation_level */ '2;1');

FILE_NAME(
/* name */ 'Cap Screw - M5x20.step',
/* time_stamp */ '2026-10-29T20:18:00-07:00',
/* author */ (''),
/* organization */ (''),
/* preprocessor_version */ 'ST-DEVELOPER v20.2',
/* originating_system */ 'Autodesk Translation Framework v15.17.0.0',
/* authorisation */ '');

FILE_SCHEMA (('AUTOMOTIVE_DESIGN { 1 0 10303 214 3 1 1 }'));
ENDSEC;

DATA;
#10=MECHANICAL_DESIGN_GEOMETRIC_PRESENTATION_REPRESENTATION('',(#249),#8428);
#148=ORIENTED_CLOSED_SHELL('',*,#3697,.F.);
#155=CONICAL_SURFACE('',#4340,0.4,0.785398163397448);
#156=CONICAL_SURFACE('',#4344,0.41,0.785398163397448);
#157=CONICAL_SURFACE('',#4348,0.26,0.463647609000806);
#158=CONICAL_SURFACE('',#4352,0.225,0.785398163397448);
#164=BREP_WITH_VOIDS('Body1',#3696,(#148));
#201=SHAPE_REPRESENTATION_RELATIONSHIP('SRR','None',#8535,#225);
#225=ADVANCED_BREP_SHAPE_REPRESENTATION('',(#164),#8424);
#249=STYLED_ITEM('',(#8712),#164);
#350=FACE_BOUND('',#997,.T.);
#465=PLANE('',#4338);
#466=PLANE('',#4346);
#467=PLANE('',#4354);
#468=PLANE('',#4355);
#469=PLANE('',#4356);
#470=PLANE('',#4357);
#471=PLANE('',#4358);
#472=PLANE('',#4359);
#473=PLANE('',#4360);
#474=PLANE('',#4361);
#475=PLANE('',#4362);
#684=FACE_OUTER_BOUND('',#992,.T.);
#685=FACE_OUTER_BOUND('',#993,.T.);
#686=FACE_OUTER_BOUND('',#994,.T.);
#687=FACE_OUTER_BOUND('',#995,.T.);
#688=FACE_OUTER_BOUND('',#996,.T.);
#689=FACE_OUTER_BOUND('',#998,.T.);
#690=FACE_OUTER_BOUND('',#999,.T.);
#691=FACE_OUTER_BOUND('',#1000,.T.);
#692=FACE_OUTER_BOUND('',#1001,.T.);
#693=FACE_OUTER_BOUND('',#1002,.T.);
#694=FACE_OUTER_BOUND('',#1003,.T.);
#695=FACE_OUTER_BOUND('',#1004,.T.);
#696=FACE_OUTER_BOUND('',#1005,.T.);
#697=FACE_OUTER_BOUND('',#1006,.T.);
#698=FACE_OUTER_BOUND('',#1007,.T.);
#699=FACE_OUTER_BOUND('',#1008,.T.);
#700=FACE_OUTER_BOUND('',#1009,.T.);
#992=EDGE_LOOP('',(#3188));
#993=EDGE_LOOP('',(#3189,#3190,#3191,#3192));
#994=EDGE_LOOP('',(#3193,#3194,#3195,#3196));
#995=EDGE_LOOP('',(#3197,#3198,#3199,#3200));
#996=EDGE_LOOP('',(#3201));
#997=EDGE_LOOP('',(#3202));
#998=EDGE_LOOP('',(#3203,#3204,#3205,#3206));
#999=EDGE_LOOP('',(#3207,#3208,#3209,#3210));
#1000=EDGE_LOOP('',(#3211,#3212,#3213,#3214));
#1001=EDGE_LOOP('',(#3215));
#1002=EDGE_LOOP('',(#3216,#3217,#3218,#3219));
#1003=EDGE_LOOP('',(#3220,#3221,#3222,#3223));
#1004=EDGE_LOOP('',(#3224,#3225,#3226,#3227));
#1005=EDGE_LOOP('',(#3228,#3229,#3230,#3231));
#1006=EDGE_LOOP('',(#3232,#3233,#3234,#3235));
#1007=EDGE_LOOP('',(#3236,#3237,#3238,#3239));
#1008=EDGE_LOOP('',(#3240,#3241,#3242,#3243,#3244,#3245));
#1009=EDGE_LOOP('',(#3246,#3247,#3248,#3249,#3250,#3251));
#1230=LINE('',#8137,#1474);
#1231=LINE('',#8141,#1475);
#1232=LINE('',#8145,#1476);
#1233=LINE('',#8152,#1477);
#1234=LINE('',#8156,#1478);
#1235=LINE('',#8160,#1479);
#1236=LINE('',#8165,#1480);
#1237=LINE('',#8167,#1481);
#1238=LINE('',#8169,#1482);
#1239=LINE('',#8170,#1483);
#1240=LINE('',#8173,#1484);
#1241=LINE('',#8175,#1485);
#1242=LINE('',#8176,#1486);
#1243=LINE('',#8179,#1487);
#1244=LINE('',#8181,#1488);
#1245=LINE('',#8182,#1489);
#1246=LINE('',#8185,#1490);
#1247=LINE('',#8187,#1491);
#1248=LINE('',#8188,#1492);
#1249=LINE('',#8191,#1493);
#1250=LINE('',#8193,#1494);
#1251=LINE('',#8194,#1495);
#1252=LINE('',#8196,#1496);
#1253=LINE('',#8197,#1497);
#1474=VECTOR('',#5376,0.4);
#1475=VECTOR('',#5381,0.425);
#1476=VECTOR('',#5386,0.41);
#1477=VECTOR('',#5395,0.26);
#1478=VECTOR('',#5400,0.25);
#1479=VECTOR('',#5405,0.225);
#1480=VECTOR('',#5410,1.);
#1481=VECTOR('',#5411,1.);
#1482=VECTOR('',#5412,1.);
#1483=VECTOR('',#5413,1.);
#1484=VECTOR('',#5416,1.);
#1485=VECTOR('',#5417,1.);
#1486=VECTOR('',#5418,1.);
#1487=VECTOR('',#5421,1.);
#1488=VECTOR('',#5422,1.);
#1489=VECTOR('',#5423,1.);
#1490=VECTOR('',#5426,1.);
#1491=VECTOR('',#5427,1.);
#1492=VECTOR('',#5428,1.);
#1493=VECTOR('',#5431,1.);
#1494=VECTOR('',#5432,1.);
#1495=VECTOR('',#5433,1.);
#1496=VECTOR('',#5436,1.);
#1497=VECTOR('',#5437,1.);
#1693=CIRCLE('',#4339,0.375);
#1694=CIRCLE('',#4341,0.425);
#1695=CIRCLE('',#4343,0.425);
#1696=CIRCLE('',#4345,0.395);
#1697=CIRCLE('',#4347,0.27);
#1698=CIRCLE('',#4349,0.24505);
#1699=CIRCLE('',#4351,0.24505);
#1700=CIRCLE('',#4353,0.2);
#1949=VERTEX_POINT('',#8132);
#1950=VERTEX_POINT('',#8135);
#1951=VERTEX_POINT('',#8139);
#1952=VERTEX_POINT('',#8143);
#1953=VERTEX_POINT('',#8147);
#1954=VERTEX_POINT('',#8150);
#1955=VERTEX_POINT('',#8154);
#1956=VERTEX_POINT('',#8158);
#1957=VERTEX_POINT('',#8163);
#1958=VERTEX_POINT('',#8164);
#1959=VERTEX_POINT('',#8166);
#1960=VERTEX_POINT('',#8168);
#1961=VERTEX_POINT('',#8172);
#1962=VERTEX_POINT('',#8174);
#1963=VERTEX_POINT('',#8178);
#1964=VERTEX_POINT('',#8180);
#1965=VERTEX_POINT('',#8184);
#1966=VERTEX_POINT('',#8186);
#1967=VERTEX_POINT('',#8190);
#1968=VERTEX_POINT('',#8192);
#2370=EDGE_CURVE('',#1949,#1949,#1693,.T.);
#2371=EDGE_CURVE('',#1950,#1950,#1694,.T.);
#2372=EDGE_CURVE('',#1950,#1949,#1230,.T.);
#2373=EDGE_CURVE('',#1951,#1951,#1695,.T.);
#2374=EDGE_CURVE('',#1951,#1950,#1231,.T.);
#2375=EDGE_CURVE('',#1952,#1952,#1696,.T.);
#2376=EDGE_CURVE('',#1952,#1951,#1232,.T.);
#2377=EDGE_CURVE('',#1953,#1953,#1697,.T.);
#2378=EDGE_CURVE('',#1954,#1954,#1698,.F.);
#2379=EDGE_CURVE('',#1954,#1953,#1233,.T.);
#2380=EDGE_CURVE('',#1955,#1955,#1699,.F.);
#2381=EDGE_CURVE('',#1955,#1954,#1234,.T.);
#2382=EDGE_CURVE('',#1956,#1956,#1700,.T.);
#2383=EDGE_CURVE('',#1956,#1955,#1235,.T.);
#2384=EDGE_CURVE('',#1957,#1958,#1236,.T.);
#2385=EDGE_CURVE('',#1958,#1959,#1237,.T.);
#2386=EDGE_CURVE('',#1959,#1960,#1238,.T.);
#2387=EDGE_CURVE('',#1957,#1960,#1239,.T.);
#2388=EDGE_CURVE('',#1958,#1961,#1240,.T.);
#2389=EDGE_CURVE('',#1961,#1962,#1241,.T.);
#2390=EDGE_CURVE('',#1962,#1959,#1242,.T.);
#2391=EDGE_CURVE('',#1961,#1963,#1243,.T.);
#2392=EDGE_CURVE('',#1963,#1964,#1244,.T.);
#2393=EDGE_CURVE('',#1964,#1962,#1245,.T.);
#2394=EDGE_CURVE('',#1963,#1965,#1246,.T.);
#2395=EDGE_CURVE('',#1965,#1966,#1247,.T.);
#2396=EDGE_CURVE('',#1966,#1964,#1248,.T.);
#2397=EDGE_CURVE('',#1965,#1967,#1249,.T.);
#2398=EDGE_CURVE('',#1967,#1968,#1250,.T.);
#2399=EDGE_CURVE('',#1968,#1966,#1251,.T.);
#2400=EDGE_CURVE('',#1967,#1957,#1252,.T.);
#2401=EDGE_CURVE('',#1960,#1968,#1253,.T.);
#3188=ORIENTED_EDGE('',*,*,#2370,.F.);
#3189=ORIENTED_EDGE('',*,*,#2371,.F.);
#3190=ORIENTED_EDGE('',*,*,#2372,.T.);
#3191=ORIENTED_EDGE('',*,*,#2370,.T.);
#3192=ORIENTED_EDGE('',*,*,#2372,.F.);
#3193=ORIENTED_EDGE('',*,*,#2373,.F.);
#3194=ORIENTED_EDGE('',*,*,#2374,.T.);
#3195=ORIENTED_EDGE('',*,*,#2371,.T.);
#3196=ORIENTED_EDGE('',*,*,#2374,.F.);
#3197=ORIENTED_EDGE('',*,*,#2375,.F.);
#3198=ORIENTED_EDGE('',*,*,#2376,.T.);
#3199=ORIENTED_EDGE('',*,*,#2373,.T.);
#3200=ORIENTED_EDGE('',*,*,#2376,.F.);
#3201=ORIENTED_EDGE('',*,*,#2375,.T.);
#3202=ORIENTED_EDGE('',*,*,#2377,.F.);
#3203=ORIENTED_EDGE('',*,*,#2378,.F.);
#3204=ORIENTED_EDGE('',*,*,#2379,.T.);
#3205=ORIENTED_EDGE('',*,*,#2377,.T.);
#3206=ORIENTED_EDGE('',*,*,#2379,.F.);
#3207=ORIENTED_EDGE('',*,*,#2380,.F.);
#3208=ORIENTED_EDGE('',*,*,#2381,.T.);
#3209=ORIENTED_EDGE('',*,*,#2378,.T.);
#3210=ORIENTED_EDGE('',*,*,#2381,.F.);
#3211=ORIENTED_EDGE('',*,*,#2382,.F.);
#3212=ORIENTED_EDGE('',*,*,#2383,.T.);
#3213=ORIENTED_EDGE('',*,*,#2380,.T.);
#3214=ORIENTED_EDGE('',*,*,#2383,.F.);
#3215=ORIENTED_EDGE('',*,*,#2382,.T.);
#3216=ORIENTED_EDGE('',*,*,#2384,.T.);
#3217=ORIENTED_EDGE('',*,*,#2385,.T.);
#3218=ORIENTED_EDGE('',*,*,#2386,.T.);
#3219=ORIENTED_EDGE('',*,*,#2387,.F.);
#3220=ORIENTED_EDGE('',*,*,#2388,.T.);
#3221=ORIENTED_EDGE('',*,*,#2389,.T.);
#3222=ORIENTED_EDGE('',*,*,#2390,.T.);
#3223=ORIENTED_EDGE('',*,*,#2385,.F.);
#3224=ORIENTED_EDGE('',*,*,#2391,.T.);
#3225=ORIENTED_EDGE('',*,*,#2392,.T.);
#3226=ORIENTED_EDGE('',*,*,#2393,.T.);
#3227=ORIENTED_EDGE('',*,*,#2389,.F.);
#3228=ORIENTED_EDGE('',*,*,#2394,.T.);
#3229=ORIENTED_EDGE('',*,*,#2395,.T.);
#3230=ORIENTED_EDGE('',*,*,#2396,.T.);
#3231=ORIENTED_EDGE('',*,*,#2392,.F.);
#3232=ORIENTED_EDGE('',*,*,#2397,.T.);
#3233=ORIENTED_EDGE('',*,*,#2398,.T.);
#3234=ORIENTED_EDGE('',*,*,#2399,.T.);
#3235=ORIENTED_EDGE('',*,*,#2395,.F.);
#3236=ORIENTED_EDGE('',*,*,#2400,.T.);
#3237=ORIENTED_EDGE('',*,*,#2387,.T.);
#3238=ORIENTED_EDGE('',*,*,#2401,.T.);
#3239=ORIENTED_EDGE('',*,*,#2398,.F.);
#3240=ORIENTED_EDGE('',*,*,#2400,.F.);
#3241=ORIENTED_EDGE('',*,*,#2397,.F.);
#3242=ORIENTED_EDGE('',*,*,#2394,.F.);
#3243=ORIENTED_EDGE('',*,*,#2391,.F.);
#3244=ORIENTED_EDGE('',*,*,#2388,.F.);
#3245=ORIENTED_EDGE('',*,*,#2384,.F.);
#3246=ORIENTED_EDGE('',*,*,#2401,.F.);
#3247=ORIENTED_EDGE('',*,*,#2386,.F.);
#3248=ORIENTED_EDGE('',*,*,#2390,.F.);
#3249=ORIENTED_EDGE('',*,*,#2393,.F.);
#3250=ORIENTED_EDGE('',*,*,#2396,.F.);
#3251=ORIENTED_EDGE('',*,*,#2399,.F.);
#3436=CYLINDRICAL_SURFACE('',#4342,0.425);
#3437=CYLINDRICAL_SURFACE('',#4350,0.24505);
#3631=ADVANCED_FACE('',(#684),#465,.T.);
#3632=ADVANCED_FACE('',(#685),#155,.T.);
#3633=ADVANCED_FACE('',(#686),#3436,.T.);
#3634=ADVANCED_FACE('',(#687),#156,.T.);
#3635=ADVANCED_FACE('',(#688,#350),#466,.T.);
#3636=ADVANCED_FACE('',(#689),#157,.T.);
#3637=ADVANCED_FACE('',(#690),#3437,.T.);
#3638=ADVANCED_FACE('',(#691),#158,.T.);
#3639=ADVANCED_FACE('',(#692),#467,.T.);
#3640=ADVANCED_FACE('',(#693),#468,.F.);
#3641=ADVANCED_FACE('',(#694),#469,.F.);
#3642=ADVANCED_FACE('',(#695),#470,.F.);
#3643=ADVANCED_FACE('',(#696),#471,.F.);
#3644=ADVANCED_FACE('',(#697),#472,.F.);
#3645=ADVANCED_FACE('',(#698),#473,.F.);
#3646=ADVANCED_FACE('',(#699),#474,.F.);
#3647=ADVANCED_FACE('',(#700),#475,.F.);
#3696=CLOSED_SHELL('',(#3631,#3632,#3633,#3634,#3635,#3636,#3637,#3638,
#3639));
#3697=CLOSED_SHELL('',(#3640,#3641,#3642,#3643,#3644,#3645,#3646,#3647));
#4337=AXIS2_PLACEMENT_3D('',#8130,#5366,#5367);
#4338=AXIS2_PLACEMENT_3D('',#8131,#5368,#5369);
#4339=AXIS2_PLACEMENT_3D('',#8133,#5370,#5371);
#4340=AXIS2_PLACEMENT_3D('',#8134,#5372,#5373);
#4341=AXIS2_PLACEMENT_3D('',#8136,#5374,#5375);
#4342=AXIS2_PLACEMENT_3D('',#8138,#5377,#5378);
#4343=AXIS2_PLACEMENT_3D('',#8140,#5379,#5380);
#4344=AXIS2_PLACEMENT_3D('',#8142,#5382,#5383);
#4345=AXIS2_PLACEMENT_3D('',#8144,#5384,#5385);
#4346=AXIS2_PLACEMENT_3D('',#8146,#5387,#5388);
#4347=AXIS2_PLACEMENT_3D('',#8148,#5389,#5390);
#4348=AXIS2_PLACEMENT_3D('',#8149,#5391,#5392);
#4349=AXIS2_PLACEMENT_3D('',#8151,#5393,#5394);
#4350=AXIS2_PLACEMENT_3D('',#8153,#5396,#5397);
#4351=AXIS2_PLACEMENT_3D('',#8155,#5398,#5399);
#4352=AXIS2_PLACEMENT_3D('',#8157,#5401,#5402);
#4353=AXIS2_PLACEMENT_3D('',#8159,#5403,#5404);
#4354=AXIS2_PLACEMENT_3D('',#8161,#5406,#5407);
#4355=AXIS2_PLACEMENT_3D('',#8162,#5408,#5409);
#4356=AXIS2_PLACEMENT_3D('',#8171,#5414,#5415);
#4357=AXIS2_PLACEMENT_3D('',#8177,#5419,#5420);
#4358=AXIS2_PLACEMENT_3D('',#8183,#5424,#5425);
#4359=AXIS2_PLACEMENT_3D('',#8189,#5429,#5430);
#4360=AXIS2_PLACEMENT_3D('',#8195,#5434,#5435);
#4361=AXIS2_PLACEMENT_3D('',#8198,#5438,#5439);
#4362=AXIS2_PLACEMENT_3D('',#8199,#5440,#5441);
#5366=DIRECTION('axis',(0.,0.,1.));
#5367=DIRECTION('refdir',(1.,0.,0.));
#5368=DIRECTION('center_axis',(0.,1.,0.));
#5369=DIRECTION('ref_axis',(0.,0.,1.));
#5370=DIRECTION('center_axis',(0.,-1.,0.));
#5371=DIRECTION('ref_axis',(1.,0.,0.));
#5372=DIRECTION('center_axis',(0.,-1.,0.));
#5373=DIRECTION('ref_axis',(1.,0.,0.));
#5374=DIRECTION('center_axis',(0.,-1.,0.));
#5375=DIRECTION('ref_axis',(1.,0.,0.));
#5376=DIRECTION('',(0.707106781186548,0.707106781186547,8.65956056235493E-17));
#5377=DIRECTION('center_axis',(0.,-1.,0.));
#5378=DIRECTION('ref_axis',(1.,0.,0.));
#5379=DIRECTION('center_axis',(0.,-1.,0.));
#5380=DIRECTION('ref_axis',(1.,0.,0.));
#5381=DIRECTION('',(0.,1.,0.));
#5382=DIRECTION('center_axis',(0.,1.,0.));
#5383=DIRECTION('ref_axis',(1.,0.,0.));
#5384=DIRECTION('center_axis',(0.,-1.,0.));
#5385=DIRECTION('ref_axis',(1.,0.,0.));
#5386=DIRECTION('',(-0.707106781186547,0.707106781186548,-8.65956056235493E-17));
#5387=DIRECTION('center_axis',(0.,-1.,0.));
#5388=DIRECTION('ref_axis',(0.,0.,-1.));
#5389=DIRECTION('center_axis',(0.,-1.,0.));
#5390=DIRECTION('ref_axis',(1.,0.,0.));
#5391=DIRECTION('center_axis',(0.,1.,0.));
#5392=DIRECTION('ref_axis',(1.,0.,0.));
#5393=DIRECTION('center_axis',(0.,1.,0.));
#5394=DIRECTION('ref_axis',(1.,0.,0.));
#5395=DIRECTION('',(-0.447213595499958,0.894427190999916,-5.47678698264203E-17));
#5396=DIRECTION('center_axis',(0.,-1.,0.));
#5397=DIRECTION('ref_axis',(1.,0.,0.));
#5398=DIRECTION('center_axis',(0.,1.,0.));
#5399=DIRECTION('ref_axis',(1.,0.,0.));
#5400=DIRECTION('',(0.,1.,0.));
#5401=DIRECTION('center_axis',(0.,1.,0.));
#5402=DIRECTION('ref_axis',(1.,0.,0.));
#5403=DIRECTION('center_axis',(0.,-1.,0.));
#5404=DIRECTION('ref_axis',(1.,0.,0.));
#5405=DIRECTION('',(-0.707106781186547,0.707106781186548,-8.65956056235493E-17));
#5406=DIRECTION('center_axis',(0.,-1.,0.));
#5407=DIRECTION('ref_axis',(0.,0.,-1.));
#5408=DIRECTION('center_axis',(0.866025403784439,0.,-0.5));
#5409=DIRECTION('ref_axis',(0.5,0.,0.866025403784439));
#5410=DIRECTION('',(-0.5,0.,-0.866025403784439));
#5411=DIRECTION('',(0.,-1.,0.));
#5412=DIRECTION('',(0.5,0.,0.866025403784439));
#5413=DIRECTION('',(0.,-1.,0.));
#5414=DIRECTION('center_axis',(1.20185167898973E-16,0.,-1.));
#5415=DIRECTION('ref_axis',(1.,0.,1.20185167898973E-16));
#5416=DIRECTION('',(-1.,0.,-1.20185167898973E-16));
#5417=DIRECTION('',(0.,-1.,0.));
#5418=DIRECTION('',(1.,0.,1.20185167898973E-16));
#5419=DIRECTION('center_axis',(-0.866025403784439,0.,-0.5));
#5420=DIRECTION('ref_axis',(0.5,0.,-0.866025403784439));
#5421=DIRECTION('',(-0.5,0.,0.866025403784439));
#5422=DIRECTION('',(0.,-1.,0.));
#5423=DIRECTION('',(0.5,0.,-0.866025403784439));
#5424=DIRECTION('center_axis',(-0.866025403784439,0.,0.5));
#5425=DIRECTION('ref_axis',(-0.5,0.,-0.866025403784439));
#5426=DIRECTION('',(0.5,0.,0.866025403784439));
#5427=DIRECTION('',(0.,-1.,0.));
#5428=DIRECTION('',(-0.5,0.,-0.866025403784439));
#5429=DIRECTION('center_axis',(-2.40370335797945E-16,0.,1.));
#5430=DIRECTION('ref_axis',(-1.,0.,-2.40370335797945E-16));
#5431=DIRECTION('',(1.,0.,2.40370335797945E-16));
#5432=DIRECTION('',(0.,-1.,0.));
#5433=DIRECTION('',(-1.,0.,-2.40370335797945E-16));
#5434=DIRECTION('center_axis',(0.866025403784439,0.,0.5));
#5435=DIRECTION('ref_axis',(-0.5,0.,0.866025403784439));
#5436=DIRECTION('',(0.5,0.,-0.866025403784439));
#5437=DIRECTION('',(-0.5,0.,0.866025403784439));
#5438=DIRECTION('center_axis',(0.,1.,0.));
#5439=DIRECTION('ref_axis',(1.,0.,0.));
#5440=DIRECTION('center_axis',(0.,-1.,0.));
#5441=DIRECTION('ref_axis',(0.,0.,-1.));
#8130=CARTESIAN_POINT('',(0.,0.,0.));
#8131=CARTESIAN_POINT('Origin',(0.375,0.5,0.));
#8132=CARTESIAN_POINT('',(-0.375,0.5,-4.59242549680257E-17));
#8133=CARTESIAN_POINT('Origin',(0.,0.5,0.));
#8134=CARTESIAN_POINT('Origin',(0.,0.475,0.));
#8135=CARTESIAN_POINT('',(-0.425,0.45,-5.20474889637625E-17));
#8136=CARTESIAN_POINT('Origin',(0.,0.45,0.));
#8137=CARTESIAN_POINT('',(-0.4,0.475,-4.89858719658941E-17));
#8138=CARTESIAN_POINT('Origin',(0.,0.24,0.));
#8139=CARTESIAN_POINT('',(-0.425,0.0299999999999998,-5.20474889637625E-17));
#8140=CARTESIAN_POINT('Origin',(0.,0.0299999999999998,0.));
#8141=CARTESIAN_POINT('',(-0.425,0.24,-5.20474889637625E-17));
#8142=CARTESIAN_POINT('Origin',(0.,0.0150000000000001,0.));
#8143=CARTESIAN_POINT('',(-0.395,4.85722573273506E-17,-4.83735485663204E-17));
#8144=CARTESIAN_POINT('Origin',(0.,0.,0.));
#8145=CARTESIAN_POINT('',(-0.41,0.0150000000000001,-5.02105187650415E-17));
#8146=CARTESIAN_POINT('Origin',(0.27,0.,0.));
#8147=CARTESIAN_POINT('',(-0.27,0.,-3.30654635769785E-17));
#8148=CARTESIAN_POINT('Origin',(0.,0.,0.));
#8149=CARTESIAN_POINT('Origin',(0.,-0.02,0.));
#8150=CARTESIAN_POINT('',(-0.24505,-0.0498999999999999,3.00099698131059E-17));
#8151=CARTESIAN_POINT('Origin',(0.,-0.0498999999999999,0.));
#8152=CARTESIAN_POINT('',(-0.26,-0.02,-3.18408167778312E-17));
#8153=CARTESIAN_POINT('Origin',(0.,-0.995,0.));
#8154=CARTESIAN_POINT('',(-0.24505,-1.95495,3.00099698131059E-17));
#8155=CARTESIAN_POINT('Origin',(0.,-1.95495,0.));
#8156=CARTESIAN_POINT('',(-0.24505,-0.995,-3.00099698131059E-17));
#8157=CARTESIAN_POINT('Origin',(0.,-1.975,0.));
#8158=CARTESIAN_POINT('',(-0.2,-2.,-2.44929359829471E-17));
#8159=CARTESIAN_POINT('Origin',(0.,-2.,0.));
#8160=CARTESIAN_POINT('',(-0.225,-1.975,-2.75545529808154E-17));
#8161=CARTESIAN_POINT('Origin',(0.,-2.,0.));
#8162=CARTESIAN_POINT('Origin',(0.115470053837925,-0.5,-0.2));
#8163=CARTESIAN_POINT('',(0.23094010767585,-0.5,0.));
#8164=CARTESIAN_POINT('',(0.115470053837925,-0.5,-0.2));
#8165=CARTESIAN_POINT('',(0.23094010767585,-0.5,0.));
#8166=CARTESIAN_POINT('',(0.115470053837925,-0.8,-0.2));
#8167=CARTESIAN_POINT('',(0.115470053837925,-0.5,-0.2));
#8168=CARTESIAN_POINT('',(0.23094010767585,-0.8,0.));
#8169=CARTESIAN_POINT('',(0.23094010767585,-0.8,0.));
#8170=CARTESIAN_POINT('',(0.23094010767585,-0.5,0.));
#8171=CARTESIAN_POINT('Origin',(-0.115470053837925,-0.5,-0.2));
#8172=CARTESIAN_POINT('',(-0.115470053837925,-0.5,-0.2));
#8173=CARTESIAN_POINT('',(0.115470053837925,-0.5,-0.2));
#8174=CARTESIAN_POINT('',(-0.115470053837925,-0.8,-0.2));
#8175=CARTESIAN_POINT('',(-0.115470053837925,-0.5,-0.2));
#8176=CARTESIAN_POINT('',(0.115470053837925,-0.8,-0.2));
#8177=CARTESIAN_POINT('Origin',(-0.23094010767585,-0.5,-2.77555756156289E-17));
#8178=CARTESIAN_POINT('',(-0.23094010767585,-0.5,-2.82820063659975E-17));
#8179=CARTESIAN_POINT('',(-0.115470053837925,-0.5,-0.2));
#8180=CARTESIAN_POINT('',(-0.23094010767585,-0.8,-2.77555756156289E-17));
#8181=CARTESIAN_POINT('',(-0.23094010767585,-0.5,-2.82820063659975E-17));
#8182=CARTESIAN_POINT('',(-0.115470053837925,-0.8,-0.2));
#8183=CARTESIAN_POINT('Origin',(-0.115470053837925,-0.5,0.2));
#8184=CARTESIAN_POINT('',(-0.115470053837925,-0.5,0.2));
#8185=CARTESIAN_POINT('',(-0.23094010767585,-0.5,-2.82820063659975E-17));
#8186=CARTESIAN_POINT('',(-0.115470053837925,-0.8,0.2));
#8187=CARTESIAN_POINT('',(-0.115470053837925,-0.5,0.2));
#8188=CARTESIAN_POINT('',(-0.23094010767585,-0.8,-2.82820063659975E-17));
#8189=CARTESIAN_POINT('Origin',(0.115470053837925,-0.5,0.2));
#8190=CARTESIAN_POINT('',(0.115470053837925,-0.5,0.2));
#8191=CARTESIAN_POINT('',(-0.115470053837925,-0.5,0.2));
#8192=CARTESIAN_POINT('',(0.115470053837925,-0.8,0.2));
#8193=CARTESIAN_POINT('',(0.115470053837925,-0.5,0.2));
#8194=CARTESIAN_POINT('',(-0.115470053837925,-0.8,0.2));
#8195=CARTESIAN_POINT('Origin',(0.23094010767585,-0.5,0.));
#8196=CARTESIAN_POINT('',(0.115470053837925,-0.5,0.2));
#8197=CARTESIAN_POINT('',(0.115470053837925,-0.8,0.2));
#8198=CARTESIAN_POINT('Origin',(0.,-0.5,0.));
#8199=CARTESIAN_POINT('Origin',(0.,-0.8,0.));
#8398=UNCERTAINTY_MEASURE_WITH_UNIT(LENGTH_MEASURE(0.001),#8429,
'DISTANCE_ACCURACY_VALUE',
'Maximum model space distance between geometric entities at asserted c
onnectivities');
#8402=UNCERTAINTY_MEASURE_WITH_UNIT(LENGTH_MEASURE(0.001),#8429,
'DISTANCE_ACCURACY_VALUE',
'Maximum model space distance between geometric entities at asserted c
onnectivities');
#8424=(
GEOMETRIC_REPRESENTATION_CONTEXT(3)
GLOBAL_UNCERTAINTY_ASSIGNED_CONTEXT((#8398))
GLOBAL_UNIT_ASSIGNED_CONTEXT((#8429,#8431,#8432))
REPRESENTATION_CONTEXT('','3D')
);
#8428=(
GEOMETRIC_REPRESENTATION_CONTEXT(3)
GLOBAL_UNCERTAINTY_ASSIGNED_CONTEXT((#8402))
GLOBAL_UNIT_ASSIGNED_CONTEXT((#8429,#8431,#8432))
REPRESENTATION_CONTEXT('','3D')
);
#8429=(
LENGTH_UNIT()
NAMED_UNIT(*)
SI_UNIT(.CENTI.,.METRE.)
);
#8431=(
NAMED_UNIT(*)
PLANE_ANGLE_UNIT()
SI_UNIT($,.RADIAN.)
);
#8432=(
NAMED_UNIT(*)
SI_UNIT($,.STERADIAN.)
SOLID_ANGLE_UNIT()
);
#8454=SHAPE_DEFINITION_REPRESENTATION(#8479,#8535);
#8479=PRODUCT_DEFINITION_SHAPE('',$,#8561);
#8535=SHAPE_REPRESENTATION('',(#4337),#8424);
#8539=PRODUCT_DEFINITION_CONTEXT('part definition',#8616,'design');
#8561=PRODUCT_DEFINITION('Cap Screw - M5x20',
'Cap Screw - M5x20',#8586,#8539);
#8586=PRODUCT_DEFINITION_FORMATION('',$,#8639);
#8616=APPLICATION_CONTEXT(
'Core Data for Automotive Mechanical Design Process');
#8617=PRODUCT_CONTEXT('part definition',#8616,'mechanical');
#8639=PRODUCT('Cap Screw - M5x20','Cap Screw - M5x20',
'Cap Screw - M5x20',(#8617));
#8706=COLOUR_RGB('Black',0.12,0.14,0.17);
#8707=FILL_AREA_STYLE_COLOUR('',#8706);
#8708=FILL_AREA_STYLE('',(#8707));
#8709=SURFACE_STYLE_FILL_AREA(#8708);
#8710=SURFACE_SIDE_STYLE('',(#8709));
#8711=SURFACE_STYLE_USAGE(.BOTH.,#8710);
#8712=PRESENTATION_STYLE_ASSIGNMENT((#8711));
ENDSEC;
END-ISO-10303-21;
